ISO-10303-21;
HEADER;
/* Generated by software containing ST-Developer
 * from STEP Tools, Inc. (www.steptools.com) 
 */

FILE_DESCRIPTION(
/* description */ (''),
/* implementation_level */ '2;1');

FILE_NAME(
/* name */ 'NUT.step',
/* time_stamp */ '2026-10-04T02:10:06-07:00',
/* author */ (''),
/* organization */ (''),
/* preprocessor_version */ 'ST-DEVELOPER v20.2',
/* originating_system */ 'Autodesk Translation Framework v15.15.0.0',
/* authorisation */ '');

FILE_SCHEMA (('AUTOMOTIVE_DESIGN { 1 0 10303 214 3 1 1 }'));
ENDSEC;

DATA;
#10=MECHANICAL_DESIGN_GEOMETRIC_PRESENTATION_REPRESENTATION('',(#150),#9668);
#83=(
BOUNDED_CURVE()
B_SPLINE_CURVE(2,(#9398,#9399,#9400),.UNSPECIFIED.,.F.,.F.)
B_SPLINE_CURVE_WITH_KNOTS((3,3),(1.40089977676118,2.46618168478736),
 .UNSPECIFIED.)
CURVE()
GEOMETRIC_REPRESENTATION_ITEM()
RATIONAL_B_SPLINE_CURVE((1.50876305611317,1.62546628464682,1.62546628464682))
REPRESENTATION_ITEM('')
);
#84=(
BOUNDED_CURVE()
B_SPLINE_CURVE(2,(#9404,#9405,#9406),.UNSPECIFIED.,.F.,.F.)
B_SPLINE_CURVE_WITH_KNOTS((3,3),(2.46617097132528,3.53145008162195),
 .UNSPECIFIED.)
CURVE()
GEOMETRIC_REPRESENTATION_ITEM()
RATIONAL_B_SPLINE_CURVE((1.6254627916221,1.6254627916221,1.50875981387633))
REPRESENTATION_ITEM('')
);
#85=(
BOUNDED_CURVE()
B_SPLINE_CURVE(2,(#9408,#9409,#9410),.UNSPECIFIED.,.F.,.F.)
B_SPLINE_CURVE_WITH_KNOTS((3,3),(1.40089186102861,2.46617097132528),
 .UNSPECIFIED.)
CURVE()
GEOMETRIC_REPRESENTATION_ITEM()
RATIONAL_B_SPLINE_CURVE((1.50875981387633,1.6254627916221,1.6254627916221))
REPRESENTATION_ITEM('')
);
#86=(
BOUNDED_CURVE()
B_SPLINE_CURVE(2,(#9413,#9414,#9415),.UNSPECIFIED.,.F.,.F.)
B_SPLINE_CURVE_WITH_KNOTS((3,3),(2.46617097132528,3.5314500816219),
 .UNSPECIFIED.)
CURVE()
GEOMETRIC_REPRESENTATION_ITEM()
RATIONAL_B_SPLINE_CURVE((1.6254627916221,1.6254627916221,1.50875981387634))
REPRESENTATION_ITEM('')
);
#87=(
BOUNDED_CURVE()
B_SPLINE_CURVE(2,(#9419,#9420,#9421),.UNSPECIFIED.,.F.,.F.)
B_SPLINE_CURVE_WITH_KNOTS((3,3),(1.40089977676118,2.46618168478736),
 .UNSPECIFIED.)
CURVE()
GEOMETRIC_REPRESENTATION_ITEM()
RATIONAL_B_SPLINE_CURVE((1.50876305611317,1.62546628464682,1.62546628464682))
REPRESENTATION_ITEM('')
);
#88=(
BOUNDED_CURVE()
B_SPLINE_CURVE(2,(#9425,#9426,#9427),.UNSPECIFIED.,.F.,.F.)
B_SPLINE_CURVE_WITH_KNOTS((3,3),(2.46617097132528,3.53145008162194),
 .UNSPECIFIED.)
CURVE()
GEOMETRIC_REPRESENTATION_ITEM()
RATIONAL_B_SPLINE_CURVE((1.6254627916221,1.6254627916221,1.50875981387633))
REPRESENTATION_ITEM('')
);
#89=(
BOUNDED_CURVE()
B_SPLINE_CURVE(2,(#9428,#9429,#9430),.UNSPECIFIED.,.F.,.F.)
B_SPLINE_CURVE_WITH_KNOTS((3,3),(1.40089186102861,2.46617097132528),
 .UNSPECIFIED.)
CURVE()
GEOMETRIC_REPRESENTATION_ITEM()
RATIONAL_B_SPLINE_CURVE((1.50875981387633,1.6254627916221,1.6254627916221))
REPRESENTATION_ITEM('')
);
#90=(
BOUNDED_CURVE()
B_SPLINE_CURVE(2,(#9431,#9432,#9433),.UNSPECIFIED.,.F.,.F.)
B_SPLINE_CURVE_WITH_KNOTS((3,3),(2.46617097132528,3.53145008162195),
 .UNSPECIFIED.)
CURVE()
GEOMETRIC_REPRESENTATION_ITEM()
RATIONAL_B_SPLINE_CURVE((1.6254627916221,1.6254627916221,1.50875981387633))
REPRESENTATION_ITEM('')
);
#91=(
BOUNDED_CURVE()
B_SPLINE_CURVE(2,(#9437,#9438,#9439),.UNSPECIFIED.,.F.,.F.)
B_SPLINE_CURVE_WITH_KNOTS((3,3),(1.4008995977322,2.46618144248253),
 .UNSPECIFIED.)
CURVE()
GEOMETRIC_REPRESENTATION_ITEM()
RATIONAL_B_SPLINE_CURVE((1.50876298278395,1.62546620564557,1.62546620564557))
REPRESENTATION_ITEM('')
);
#92=(
BOUNDED_CURVE()
B_SPLINE_CURVE(2,(#9443,#9444,#9445),.UNSPECIFIED.,.F.,.F.)
B_SPLINE_CURVE_WITH_KNOTS((3,3),(2.46618137387007,3.53146320070284),
 .UNSPECIFIED.)
CURVE()
GEOMETRIC_REPRESENTATION_ITEM()
RATIONAL_B_SPLINE_CURVE((1.62546618327512,1.62546618327512,1.50876296201962))
REPRESENTATION_ITEM('')
);
#93=(
BOUNDED_CURVE()
B_SPLINE_CURVE(2,(#9446,#9447,#9448),.UNSPECIFIED.,.F.,.F.)
B_SPLINE_CURVE_WITH_KNOTS((3,3),(1.4008995470373,2.46618137387007),
 .UNSPECIFIED.)
CURVE()
GEOMETRIC_REPRESENTATION_ITEM()
RATIONAL_B_SPLINE_CURVE((1.50876296201962,1.62546618327511,1.62546618327511))
REPRESENTATION_ITEM('')
);
#94=(
BOUNDED_CURVE()
B_SPLINE_CURVE(2,(#9449,#9450,#9451),.UNSPECIFIED.,.F.,.F.)
B_SPLINE_CURVE_WITH_KNOTS((3,3),(2.46617097132528,3.53145008162195),
 .UNSPECIFIED.)
CURVE()
GEOMETRIC_REPRESENTATION_ITEM()
RATIONAL_B_SPLINE_CURVE((1.6254627916221,1.6254627916221,1.50875981387633))
REPRESENTATION_ITEM('')
);
#95=(
BOUNDED_CURVE()
B_SPLINE_CURVE(2,(#9455,#9456,#9457),.UNSPECIFIED.,.F.,.F.)
B_SPLINE_CURVE_WITH_KNOTS((3,3),(1.40089977676118,2.46618168478736),
 .UNSPECIFIED.)
CURVE()
GEOMETRIC_REPRESENTATION_ITEM()
RATIONAL_B_SPLINE_CURVE((1.50876305611317,1.62546628464682,1.62546628464682))
REPRESENTATION_ITEM('')
);
#96=(
BOUNDED_CURVE()
B_SPLINE_CURVE(2,(#9461,#9462,#9463),.UNSPECIFIED.,.F.,.F.)
B_SPLINE_CURVE_WITH_KNOTS((3,3),(2.46617097132528,3.53145008162195),
 .UNSPECIFIED.)
CURVE()
GEOMETRIC_REPRESENTATION_ITEM()
RATIONAL_B_SPLINE_CURVE((1.6254627916221,1.6254627916221,1.50875981387633))
REPRESENTATION_ITEM('')
);
#97=(
BOUNDED_CURVE()
B_SPLINE_CURVE(2,(#9464,#9465,#9466),.UNSPECIFIED.,.F.,.F.)
B_SPLINE_CURVE_WITH_KNOTS((3,3),(1.40089186102861,2.46617097132528),
 .UNSPECIFIED.)
CURVE()
GEOMETRIC_REPRESENTATION_ITEM()
RATIONAL_B_SPLINE_CURVE((1.50875981387633,1.6254627916221,1.6254627916221))
REPRESENTATION_ITEM('')
);
#98=(
BOUNDED_CURVE()
B_SPLINE_CURVE(2,(#9467,#9468,#9469),.UNSPECIFIED.,.F.,.F.)
B_SPLINE_CURVE_WITH_KNOTS((3,3),(2.46617097132528,3.53145008162195),
 .UNSPECIFIED.)
CURVE()
GEOMETRIC_REPRESENTATION_ITEM()
RATIONAL_B_SPLINE_CURVE((1.62546279162209,1.62546279162209,1.50875981387633))
REPRESENTATION_ITEM('')
);
#99=(
BOUNDED_CURVE()
B_SPLINE_CURVE(2,(#9473,#9474,#9475),.UNSPECIFIED.,.F.,.F.)
B_SPLINE_CURVE_WITH_KNOTS((3,3),(1.40089977676118,2.46618168478736),
 .UNSPECIFIED.)
CURVE()
GEOMETRIC_REPRESENTATION_ITEM()
RATIONAL_B_SPLINE_CURVE((1.50876305611317,1.62546628464682,1.62546628464682))
REPRESENTATION_ITEM('')
);
#100=(
BOUNDED_CURVE()
B_SPLINE_CURVE(2,(#9479,#9480,#9481),.UNSPECIFIED.,.F.,.F.)
B_SPLINE_CURVE_WITH_KNOTS((3,3),(2.46617097132528,3.53145008162194),
 .UNSPECIFIED.)
CURVE()
GEOMETRIC_REPRESENTATION_ITEM()
RATIONAL_B_SPLINE_CURVE((1.6254627916221,1.6254627916221,1.50875981387634))
REPRESENTATION_ITEM('')
);
#101=(
BOUNDED_CURVE()
B_SPLINE_CURVE(2,(#9482,#9483,#9484),.UNSPECIFIED.,.F.,.F.)
B_SPLINE_CURVE_WITH_KNOTS((3,3),(1.40089186102861,2.46617097132528),
 .UNSPECIFIED.)
CURVE()
GEOMETRIC_REPRESENTATION_ITEM()
RATIONAL_B_SPLINE_CURVE((1.50875981387633,1.6254627916221,1.6254627916221))
REPRESENTATION_ITEM('')
);
#102=(
BOUNDED_CURVE()
B_SPLINE_CURVE(2,(#9485,#9486,#9487),.UNSPECIFIED.,.F.,.F.)
B_SPLINE_CURVE_WITH_KNOTS((3,3),(2.46617097132529,3.53145008162195),
 .UNSPECIFIED.)
CURVE()
GEOMETRIC_REPRESENTATION_ITEM()
RATIONAL_B_SPLINE_CURVE((1.6254627916221,1.6254627916221,1.50875981387633))
REPRESENTATION_ITEM('')
);
#103=(
BOUNDED_CURVE()
B_SPLINE_CURVE(2,(#9490,#9491,#9492),.UNSPECIFIED.,.F.,.F.)
B_SPLINE_CURVE_WITH_KNOTS((3,3),(1.4008995977321,2.46618144248253),
 .UNSPECIFIED.)
CURVE()
GEOMETRIC_REPRESENTATION_ITEM()
RATIONAL_B_SPLINE_CURVE((1.50876298278393,1.62546620564557,1.62546620564557))
REPRESENTATION_ITEM('')
);
#104=(
BOUNDED_CURVE()
B_SPLINE_CURVE(2,(#9494,#9495,#9496),.UNSPECIFIED.,.F.,.F.)
B_SPLINE_CURVE_WITH_KNOTS((3,3),(2.46618137387007,3.53146320070284),
 .UNSPECIFIED.)
CURVE()
GEOMETRIC_REPRESENTATION_ITEM()
RATIONAL_B_SPLINE_CURVE((1.62546618327512,1.62546618327512,1.50876296201962))
REPRESENTATION_ITEM('')
);
#105=(
BOUNDED_CURVE()
B_SPLINE_CURVE(2,(#9497,#9498,#9499),.UNSPECIFIED.,.F.,.F.)
B_SPLINE_CURVE_WITH_KNOTS((3,3),(1.4008995470373,2.46618137387007),
 .UNSPECIFIED.)
CURVE()
GEOMETRIC_REPRESENTATION_ITEM()
RATIONAL_B_SPLINE_CURVE((1.50876296201962,1.62546618327511,1.62546618327511))
REPRESENTATION_ITEM('')
);
#106=(
BOUNDED_CURVE()
B_SPLINE_CURVE(2,(#9500,#9501,#9502),.UNSPECIFIED.,.F.,.F.)
B_SPLINE_CURVE_WITH_KNOTS((3,3),(2.46617097132528,3.53145008162195),
 .UNSPECIFIED.)
CURVE()
GEOMETRIC_REPRESENTATION_ITEM()
RATIONAL_B_SPLINE_CURVE((1.6254627916221,1.6254627916221,1.50875981387633))
REPRESENTATION_ITEM('')
);
#128=SHAPE_REPRESENTATION_RELATIONSHIP('SRR','None',#9721,#139);
#139=ADVANCED_BREP_SHAPE_REPRESENTATION('',(#161),#9666);
#150=STYLED_ITEM('',(#9775),#161);
#161=MANIFOLD_SOLID_BREP('Body1',#3890);
#177=CONICAL_SURFACE('',#4418,10.3923048454133,0.78539816339745);
#178=CONICAL_SURFACE('',#4419,10.3923048454133,0.78539816339745);
#179=CONICAL_SURFACE('',#4420,10.3923048454133,0.78539816339745);
#180=CONICAL_SURFACE('',#4421,10.3923048454133,0.78539816339745);
#181=CONICAL_SURFACE('',#4422,10.3923048454133,0.78539816339745);
#182=CONICAL_SURFACE('',#4423,10.3923048454133,0.78539816339745);
#183=CONICAL_SURFACE('',#4424,10.3923048454133,0.78539816339745);
#184=CONICAL_SURFACE('',#4425,10.3923048454133,0.78539816339745);
#185=CONICAL_SURFACE('',#4426,10.3923048454133,0.78539816339745);
#186=CONICAL_SURFACE('',#4427,10.3923048454133,0.78539816339745);
#187=CONICAL_SURFACE('',#4428,10.3923048454133,0.78539816339745);
#188=CONICAL_SURFACE('',#4429,10.3923048454133,0.78539816339745);
#265=FACE_BOUND('',#1296,.T.);
#266=FACE_BOUND('',#1298,.T.);
#354=PLANE('',#4395);
#355=PLANE('',#4396);
#356=PLANE('',#4397);
#357=PLANE('',#4398);
#358=PLANE('',#4399);
#359=PLANE('',#4400);
#360=PLANE('',#4401);
#361=PLANE('',#4409);
#542=LINE('',#9402,#733);
#543=LINE('',#9412,#734);
#544=LINE('',#9423,#735);
#545=LINE('',#9441,#736);
#546=LINE('',#9459,#737);
#547=LINE('',#9477,#738);
#548=LINE('',#9522,#739);
#733=VECTOR('',#5404,8.78460969082654);
#734=VECTOR('',#5405,8.78460969082657);
#735=VECTOR('',#5408,8.78460969082654);
#736=VECTOR('',#5411,8.78460969082653);
#737=VECTOR('',#5414,8.78460969082654);
#738=VECTOR('',#5417,8.78460969082654);
#739=VECTOR('',#5454,6.);
#808=CYLINDRICAL_SURFACE('',#4417,6.);
#996=FACE_OUTER_BOUND('',#1289,.T.);
#997=FACE_OUTER_BOUND('',#1290,.T.);
#998=FACE_OUTER_BOUND('',#1291,.T.);
#999=FACE_OUTER_BOUND('',#1292,.T.);
#1000=FACE_OUTER_BOUND('',#1293,.T.);
#1001=FACE_OUTER_BOUND('',#1294,.T.);
#1002=FACE_OUTER_BOUND('',#1295,.T.);
#1003=FACE_OUTER_BOUND('',#1297,.T.);
#1004=FACE_OUTER_BOUND('',#1299,.T.);
#1005=FACE_OUTER_BOUND('',#1300,.T.);
#1006=FACE_OUTER_BOUND('',#1301,.T.);
#1007=FACE_OUTER_BOUND('',#1302,.T.);
#1008=FACE_OUTER_BOUND('',#1303,.T.);
#1009=FACE_OUTER_BOUND('',#1304,.T.);
#1010=FACE_OUTER_BOUND('',#1305,.T.);
#1011=FACE_OUTER_BOUND('',#1306,.T.);
#1012=FACE_OUTER_BOUND('',#1307,.T.);
#1013=FACE_OUTER_BOUND('',#1308,.T.);
#1014=FACE_OUTER_BOUND('',#1309,.T.);
#1015=FACE_OUTER_BOUND('',#1310,.T.);
#1016=FACE_OUTER_BOUND('',#1311,.T.);
#1289=EDGE_LOOP('',(#3479,#3480,#3481,#3482,#3483,#3484));
#1290=EDGE_LOOP('',(#3485,#3486,#3487,#3488,#3489,#3490));
#1291=EDGE_LOOP('',(#3491,#3492,#3493,#3494,#3495,#3496));
#1292=EDGE_LOOP('',(#3497,#3498,#3499,#3500,#3501,#3502));
#1293=EDGE_LOOP('',(#3503,#3504,#3505,#3506,#3507,#3508));
#1294=EDGE_LOOP('',(#3509,#3510,#3511,#3512,#3513,#3514));
#1295=EDGE_LOOP('',(#3515,#3516,#3517,#3518,#3519,#3520));
#1296=EDGE_LOOP('',(#3521));
#1297=EDGE_LOOP('',(#3522,#3523,#3524,#3525,#3526,#3527));
#1298=EDGE_LOOP('',(#3528));
#1299=EDGE_LOOP('',(#3529,#3530,#3531,#3532));
#1300=EDGE_LOOP('',(#3533,#3534,#3535));
#1301=EDGE_LOOP('',(#3536,#3537,#3538));
#1302=EDGE_LOOP('',(#3539,#3540,#3541));
#1303=EDGE_LOOP('',(#3542,#3543,#3544));
#1304=EDGE_LOOP('',(#3545,#3546,#3547));
#1305=EDGE_LOOP('',(#3548,#3549,#3550));
#1306=EDGE_LOOP('',(#3551,#3552,#3553));
#1307=EDGE_LOOP('',(#3554,#3555,#3556));
#1308=EDGE_LOOP('',(#3557,#3558,#3559));
#1309=EDGE_LOOP('',(#3560,#3561,#3562));
#1310=EDGE_LOOP('',(#3563,#3564,#3565));
#1311=EDGE_LOOP('',(#3566,#3567,#3568));
#1619=CIRCLE('',#4402,10.3923048454133);
#1620=CIRCLE('',#4403,10.3923048454133);
#1621=CIRCLE('',#4404,10.3923048454133);
#1622=CIRCLE('',#4405,10.3923048454133);
#1623=CIRCLE('',#4406,10.3923048454133);
#1624=CIRCLE('',#4407,10.3923048454133);
#1625=CIRCLE('',#4408,6.);
#1626=CIRCLE('',#4410,10.3923048454133);
#1627=CIRCLE('',#4411,10.3923048454133);
#1628=CIRCLE('',#4412,10.3923048454133);
#1629=CIRCLE('',#4413,10.3923048454133);
#1630=CIRCLE('',#4414,10.3923048454133);
#1631=CIRCLE('',#4415,10.3923048454133);
#1632=CIRCLE('',#4416,6.);
#1948=VERTEX_POINT('',#9396);
#1949=VERTEX_POINT('',#9397);
#1950=VERTEX_POINT('',#9401);
#1951=VERTEX_POINT('',#9403);
#1952=VERTEX_POINT('',#9407);
#1953=VERTEX_POINT('',#9411);
#1954=VERTEX_POINT('',#9417);
#1955=VERTEX_POINT('',#9418);
#1956=VERTEX_POINT('',#9422);
#1957=VERTEX_POINT('',#9424);
#1958=VERTEX_POINT('',#9435);
#1959=VERTEX_POINT('',#9436);
#1960=VERTEX_POINT('',#9440);
#1961=VERTEX_POINT('',#9442);
#1962=VERTEX_POINT('',#9453);
#1963=VERTEX_POINT('',#9454);
#1964=VERTEX_POINT('',#9458);
#1965=VERTEX_POINT('',#9460);
#1966=VERTEX_POINT('',#9471);
#1967=VERTEX_POINT('',#9472);
#1968=VERTEX_POINT('',#9476);
#1969=VERTEX_POINT('',#9478);
#1970=VERTEX_POINT('',#9489);
#1971=VERTEX_POINT('',#9493);
#1972=VERTEX_POINT('',#9510);
#1973=VERTEX_POINT('',#9519);
#2463=EDGE_CURVE('',#1948,#1949,#83,.T.);
#2464=EDGE_CURVE('',#1950,#1948,#542,.T.);
#2465=EDGE_CURVE('',#1951,#1950,#84,.T.);
#2466=EDGE_CURVE('',#1952,#1951,#85,.T.);
#2467=EDGE_CURVE('',#1952,#1953,#543,.T.);
#2468=EDGE_CURVE('',#1949,#1953,#86,.T.);
#2469=EDGE_CURVE('',#1954,#1955,#87,.T.);
#2470=EDGE_CURVE('',#1956,#1954,#544,.T.);
#2471=EDGE_CURVE('',#1957,#1956,#88,.T.);
#2472=EDGE_CURVE('',#1950,#1957,#89,.T.);
#2473=EDGE_CURVE('',#1955,#1948,#90,.T.);
#2474=EDGE_CURVE('',#1958,#1959,#91,.T.);
#2475=EDGE_CURVE('',#1960,#1958,#545,.T.);
#2476=EDGE_CURVE('',#1961,#1960,#92,.T.);
#2477=EDGE_CURVE('',#1956,#1961,#93,.T.);
#2478=EDGE_CURVE('',#1959,#1954,#94,.T.);
#2479=EDGE_CURVE('',#1962,#1963,#95,.T.);
#2480=EDGE_CURVE('',#1964,#1962,#546,.T.);
#2481=EDGE_CURVE('',#1965,#1964,#96,.T.);
#2482=EDGE_CURVE('',#1960,#1965,#97,.T.);
#2483=EDGE_CURVE('',#1963,#1958,#98,.T.);
#2484=EDGE_CURVE('',#1966,#1967,#99,.T.);
#2485=EDGE_CURVE('',#1968,#1966,#547,.T.);
#2486=EDGE_CURVE('',#1969,#1968,#100,.T.);
#2487=EDGE_CURVE('',#1964,#1969,#101,.T.);
#2488=EDGE_CURVE('',#1967,#1962,#102,.T.);
#2489=EDGE_CURVE('',#1953,#1970,#103,.T.);
#2490=EDGE_CURVE('',#1971,#1952,#104,.T.);
#2491=EDGE_CURVE('',#1968,#1971,#105,.T.);
#2492=EDGE_CURVE('',#1970,#1966,#106,.T.);
#2493=EDGE_CURVE('',#1970,#1949,#1619,.T.);
#2494=EDGE_CURVE('',#1967,#1970,#1620,.T.);
#2495=EDGE_CURVE('',#1963,#1967,#1621,.T.);
#2496=EDGE_CURVE('',#1959,#1963,#1622,.T.);
#2497=EDGE_CURVE('',#1959,#1955,#1623,.T.);
#2498=EDGE_CURVE('',#1949,#1955,#1624,.T.);
#2499=EDGE_CURVE('',#1972,#1972,#1625,.T.);
#2500=EDGE_CURVE('',#1969,#1971,#1626,.T.);
#2501=EDGE_CURVE('',#1971,#1951,#1627,.T.);
#2502=EDGE_CURVE('',#1951,#1957,#1628,.T.);
#2503=EDGE_CURVE('',#1957,#1961,#1629,.T.);
#2504=EDGE_CURVE('',#1961,#1965,#1630,.T.);
#2505=EDGE_CURVE('',#1965,#1969,#1631,.T.);
#2506=EDGE_CURVE('',#1973,#1973,#1632,.T.);
#2507=EDGE_CURVE('',#1973,#1972,#548,.T.);
#3479=ORIENTED_EDGE('',*,*,#2463,.F.);
#3480=ORIENTED_EDGE('',*,*,#2464,.F.);
#3481=ORIENTED_EDGE('',*,*,#2465,.F.);
#3482=ORIENTED_EDGE('',*,*,#2466,.F.);
#3483=ORIENTED_EDGE('',*,*,#2467,.T.);
#3484=ORIENTED_EDGE('',*,*,#2468,.F.);
#3485=ORIENTED_EDGE('',*,*,#2469,.F.);
#3486=ORIENTED_EDGE('',*,*,#2470,.F.);
#3487=ORIENTED_EDGE('',*,*,#2471,.F.);
#3488=ORIENTED_EDGE('',*,*,#2472,.F.);
#3489=ORIENTED_EDGE('',*,*,#2464,.T.);
#3490=ORIENTED_EDGE('',*,*,#2473,.F.);
#3491=ORIENTED_EDGE('',*,*,#2474,.F.);
#3492=ORIENTED_EDGE('',*,*,#2475,.F.);
#3493=ORIENTED_EDGE('',*,*,#2476,.F.);
#3494=ORIENTED_EDGE('',*,*,#2477,.F.);
#3495=ORIENTED_EDGE('',*,*,#2470,.T.);
#3496=ORIENTED_EDGE('',*,*,#2478,.F.);
#3497=ORIENTED_EDGE('',*,*,#2479,.F.);
#3498=ORIENTED_EDGE('',*,*,#2480,.F.);
#3499=ORIENTED_EDGE('',*,*,#2481,.F.);
#3500=ORIENTED_EDGE('',*,*,#2482,.F.);
#3501=ORIENTED_EDGE('',*,*,#2475,.T.);
#3502=ORIENTED_EDGE('',*,*,#2483,.F.);
#3503=ORIENTED_EDGE('',*,*,#2484,.F.);
#3504=ORIENTED_EDGE('',*,*,#2485,.F.);
#3505=ORIENTED_EDGE('',*,*,#2486,.F.);
#3506=ORIENTED_EDGE('',*,*,#2487,.F.);
#3507=ORIENTED_EDGE('',*,*,#2480,.T.);
#3508=ORIENTED_EDGE('',*,*,#2488,.F.);
#3509=ORIENTED_EDGE('',*,*,#2489,.F.);
#3510=ORIENTED_EDGE('',*,*,#2467,.F.);
#3511=ORIENTED_EDGE('',*,*,#2490,.F.);
#3512=ORIENTED_EDGE('',*,*,#2491,.F.);
#3513=ORIENTED_EDGE('',*,*,#2485,.T.);
#3514=ORIENTED_EDGE('',*,*,#2492,.F.);
#3515=ORIENTED_EDGE('',*,*,#2493,.F.);
#3516=ORIENTED_EDGE('',*,*,#2494,.F.);
#3517=ORIENTED_EDGE('',*,*,#2495,.F.);
#3518=ORIENTED_EDGE('',*,*,#2496,.F.);
#3519=ORIENTED_EDGE('',*,*,#2497,.T.);
#3520=ORIENTED_EDGE('',*,*,#2498,.F.);
#3521=ORIENTED_EDGE('',*,*,#2499,.T.);
#3522=ORIENTED_EDGE('',*,*,#2500,.T.);
#3523=ORIENTED_EDGE('',*,*,#2501,.T.);
#3524=ORIENTED_EDGE('',*,*,#2502,.T.);
#3525=ORIENTED_EDGE('',*,*,#2503,.T.);
#3526=ORIENTED_EDGE('',*,*,#2504,.T.);
#3527=ORIENTED_EDGE('',*,*,#2505,.T.);
#3528=ORIENTED_EDGE('',*,*,#2506,.F.);
#3529=ORIENTED_EDGE('',*,*,#2506,.T.);
#3530=ORIENTED_EDGE('',*,*,#2507,.T.);
#3531=ORIENTED_EDGE('',*,*,#2499,.F.);
#3532=ORIENTED_EDGE('',*,*,#2507,.F.);
#3533=ORIENTED_EDGE('',*,*,#2466,.T.);
#3534=ORIENTED_EDGE('',*,*,#2501,.F.);
#3535=ORIENTED_EDGE('',*,*,#2490,.T.);
#3536=ORIENTED_EDGE('',*,*,#2486,.T.);
#3537=ORIENTED_EDGE('',*,*,#2491,.T.);
#3538=ORIENTED_EDGE('',*,*,#2500,.F.);
#3539=ORIENTED_EDGE('',*,*,#2481,.T.);
#3540=ORIENTED_EDGE('',*,*,#2487,.T.);
#3541=ORIENTED_EDGE('',*,*,#2505,.F.);
#3542=ORIENTED_EDGE('',*,*,#2476,.T.);
#3543=ORIENTED_EDGE('',*,*,#2482,.T.);
#3544=ORIENTED_EDGE('',*,*,#2504,.F.);
#3545=ORIENTED_EDGE('',*,*,#2471,.T.);
#3546=ORIENTED_EDGE('',*,*,#2477,.T.);
#3547=ORIENTED_EDGE('',*,*,#2503,.F.);
#3548=ORIENTED_EDGE('',*,*,#2465,.T.);
#3549=ORIENTED_EDGE('',*,*,#2472,.T.);
#3550=ORIENTED_EDGE('',*,*,#2502,.F.);
#3551=ORIENTED_EDGE('',*,*,#2484,.T.);
#3552=ORIENTED_EDGE('',*,*,#2494,.T.);
#3553=ORIENTED_EDGE('',*,*,#2492,.T.);
#3554=ORIENTED_EDGE('',*,*,#2479,.T.);
#3555=ORIENTED_EDGE('',*,*,#2495,.T.);
#3556=ORIENTED_EDGE('',*,*,#2488,.T.);
#3557=ORIENTED_EDGE('',*,*,#2474,.T.);
#3558=ORIENTED_EDGE('',*,*,#2496,.T.);
#3559=ORIENTED_EDGE('',*,*,#2483,.T.);
#3560=ORIENTED_EDGE('',*,*,#2478,.T.);
#3561=ORIENTED_EDGE('',*,*,#2469,.T.);
#3562=ORIENTED_EDGE('',*,*,#2497,.F.);
#3563=ORIENTED_EDGE('',*,*,#2473,.T.);
#3564=ORIENTED_EDGE('',*,*,#2463,.T.);
#3565=ORIENTED_EDGE('',*,*,#2498,.T.);
#3566=ORIENTED_EDGE('',*,*,#2468,.T.);
#3567=ORIENTED_EDGE('',*,*,#2489,.T.);
#3568=ORIENTED_EDGE('',*,*,#2493,.T.);
#3844=ADVANCED_FACE('',(#996),#354,.F.);
#3845=ADVANCED_FACE('',(#997),#355,.F.);
#3846=ADVANCED_FACE('',(#998),#356,.F.);
#3847=ADVANCED_FACE('',(#999),#357,.F.);
#3848=ADVANCED_FACE('',(#1000),#358,.F.);
#3849=ADVANCED_FACE('',(#1001),#359,.F.);
#3850=ADVANCED_FACE('',(#1002,#265),#360,.F.);
#3851=ADVANCED_FACE('',(#1003,#266),#361,.T.);
#3852=ADVANCED_FACE('',(#1004),#808,.F.);
#3853=ADVANCED_FACE('',(#1005),#177,.T.);
#3854=ADVANCED_FACE('',(#1006),#178,.T.);
#3855=ADVANCED_FACE('',(#1007),#179,.T.);
#3856=ADVANCED_FACE('',(#1008),#180,.T.);
#3857=ADVANCED_FACE('',(#1009),#181,.T.);
#3858=ADVANCED_FACE('',(#1010),#182,.T.);
#3859=ADVANCED_FACE('',(#1011),#183,.T.);
#3860=ADVANCED_FACE('',(#1012),#184,.T.);
#3861=ADVANCED_FACE('',(#1013),#185,.T.);
#3862=ADVANCED_FACE('',(#1014),#186,.T.);
#3863=ADVANCED_FACE('',(#1015),#187,.T.);
#3864=ADVANCED_FACE('',(#1016),#188,.T.);
#3890=CLOSED_SHELL('',(#3844,#3845,#3846,#3847,#3848,#3849,#3850,#3851,
#3852,#3853,#3854,#3855,#3856,#3857,#3858,#3859,#3860,#3861,#3862,#3863,
#3864));
#4394=AXIS2_PLACEMENT_3D('',#9394,#5400,#5401);
#4395=AXIS2_PLACEMENT_3D('',#9395,#5402,#5403);
#4396=AXIS2_PLACEMENT_3D('',#9416,#5406,#5407);
#4397=AXIS2_PLACEMENT_3D('',#9434,#5409,#5410);
#4398=AXIS2_PLACEMENT_3D('',#9452,#5412,#5413);
#4399=AXIS2_PLACEMENT_3D('',#9470,#5415,#5416);
#4400=AXIS2_PLACEMENT_3D('',#9488,#5418,#5419);
#4401=AXIS2_PLACEMENT_3D('',#9503,#5420,#5421);
#4402=AXIS2_PLACEMENT_3D('',#9504,#5422,#5423);
#4403=AXIS2_PLACEMENT_3D('',#9505,#5424,#5425);
#4404=AXIS2_PLACEMENT_3D('',#9506,#5426,#5427);
#4405=AXIS2_PLACEMENT_3D('',#9507,#5428,#5429);
#4406=AXIS2_PLACEMENT_3D('',#9508,#5430,#5431);
#4407=AXIS2_PLACEMENT_3D('',#9509,#5432,#5433);
#4408=AXIS2_PLACEMENT_3D('',#9511,#5434,#5435);
#4409=AXIS2_PLACEMENT_3D('',#9512,#5436,#5437);
#4410=AXIS2_PLACEMENT_3D('',#9513,#5438,#5439);
#4411=AXIS2_PLACEMENT_3D('',#9514,#5440,#5441);
#4412=AXIS2_PLACEMENT_3D('',#9515,#5442,#5443);
#4413=AXIS2_PLACEMENT_3D('',#9516,#5444,#5445);
#4414=AXIS2_PLACEMENT_3D('',#9517,#5446,#5447);
#4415=AXIS2_PLACEMENT_3D('',#9518,#5448,#5449);
#4416=AXIS2_PLACEMENT_3D('',#9520,#5450,#5451);
#4417=AXIS2_PLACEMENT_3D('',#9521,#5452,#5453);
#4418=AXIS2_PLACEMENT_3D('',#9523,#5455,#5456);
#4419=AXIS2_PLACEMENT_3D('',#9524,#5457,#5458);
#4420=AXIS2_PLACEMENT_3D('',#9525,#5459,#5460);
#4421=AXIS2_PLACEMENT_3D('',#9526,#5461,#5462);
#4422=AXIS2_PLACEMENT_3D('',#9527,#5463,#5464);
#4423=AXIS2_PLACEMENT_3D('',#9528,#5465,#5466);
#4424=AXIS2_PLACEMENT_3D('',#9529,#5467,#5468);
#4425=AXIS2_PLACEMENT_3D('',#9530,#5469,#5470);
#4426=AXIS2_PLACEMENT_3D('',#9531,#5471,#5472);
#4427=AXIS2_PLACEMENT_3D('',#9532,#5473,#5474);
#4428=AXIS2_PLACEMENT_3D('',#9533,#5475,#5476);
#4429=AXIS2_PLACEMENT_3D('',#9534,#5477,#5478);
#5400=DIRECTION('axis',(0.,0.,1.));
#5401=DIRECTION('refdir',(1.,0.,0.));
#5402=DIRECTION('center_axis',(-0.866025403784439,0.,-0.5));
#5403=DIRECTION('ref_axis',(-0.5,0.,0.866025403784439));
#5404=DIRECTION('',(0.,-1.,0.));
#5405=DIRECTION('',(0.,-1.,0.));
#5406=DIRECTION('center_axis',(-0.866025403784439,0.,0.5));
#5407=DIRECTION('ref_axis',(0.5,0.,0.866025403784439));
#5408=DIRECTION('',(0.,-1.,0.));
#5409=DIRECTION('center_axis',(0.,0.,1.));
#5410=DIRECTION('ref_axis',(1.,0.,0.));
#5411=DIRECTION('',(0.,-1.,0.));
#5412=DIRECTION('center_axis',(0.866025403784439,0.,0.5));
#5413=DIRECTION('ref_axis',(0.5,0.,-0.866025403784439));
#5414=DIRECTION('',(0.,-1.,0.));
#5415=DIRECTION('center_axis',(0.866025403784439,0.,-0.5));
#5416=DIRECTION('ref_axis',(-0.5,0.,-0.866025403784439));
#5417=DIRECTION('',(0.,-1.,0.));
#5418=DIRECTION('center_axis',(1.44560289664734E-16,0.,-1.));
#5419=DIRECTION('ref_axis',(-1.,0.,-1.44560289664734E-16));
#5420=DIRECTION('center_axis',(0.,1.,0.));
#5421=DIRECTION('ref_axis',(0.,0.,1.));
#5422=DIRECTION('center_axis',(0.,1.,0.));
#5423=DIRECTION('ref_axis',(0.,0.,1.));
#5424=DIRECTION('center_axis',(0.,1.,0.));
#5425=DIRECTION('ref_axis',(0.,0.,1.));
#5426=DIRECTION('center_axis',(0.,1.,0.));
#5427=DIRECTION('ref_axis',(0.,0.,1.));
#5428=DIRECTION('center_axis',(0.,1.,0.));
#5429=DIRECTION('ref_axis',(0.,0.,1.));
#5430=DIRECTION('center_axis',(0.,-1.,0.));
#5431=DIRECTION('ref_axis',(0.,0.,-1.));
#5432=DIRECTION('center_axis',(0.,1.,0.));
#5433=DIRECTION('ref_axis',(0.,0.,1.));
#5434=DIRECTION('center_axis',(0.,1.,0.));
#5435=DIRECTION('ref_axis',(0.,0.,1.));
#5436=DIRECTION('center_axis',(0.,1.,0.));
#5437=DIRECTION('ref_axis',(0.,0.,1.));
#5438=DIRECTION('center_axis',(0.,1.,0.));
#5439=DIRECTION('ref_axis',(0.,0.,1.));
#5440=DIRECTION('center_axis',(0.,1.,0.));
#5441=DIRECTION('ref_axis',(0.,0.,1.));
#5442=DIRECTION('center_axis',(0.,1.,0.));
#5443=DIRECTION('ref_axis',(0.,0.,1.));
#5444=DIRECTION('center_axis',(0.,1.,0.));
#5445=DIRECTION('ref_axis',(0.,0.,1.));
#5446=DIRECTION('center_axis',(0.,1.,0.));
#5447=DIRECTION('ref_axis',(0.,0.,1.));
#5448=DIRECTION('center_axis',(0.,1.,0.));
#5449=DIRECTION('ref_axis',(0.,0.,1.));
#5450=DIRECTION('center_axis',(0.,1.,0.));
#5451=DIRECTION('ref_axis',(0.,0.,1.));
#5452=DIRECTION('center_axis',(0.,-1.,0.));
#5453=DIRECTION('ref_axis',(0.,0.,-1.));
#5454=DIRECTION('',(0.,-1.,0.));
#5455=DIRECTION('center_axis',(0.,-1.,0.));
#5456=DIRECTION('ref_axis',(0.,0.,1.));
#5457=DIRECTION('center_axis',(0.,-1.,0.));
#5458=DIRECTION('ref_axis',(0.,0.,1.));
#5459=DIRECTION('center_axis',(0.,-1.,0.));
#5460=DIRECTION('ref_axis',(0.,0.,1.));
#5461=DIRECTION('center_axis',(0.,-1.,0.));
#5462=DIRECTION('ref_axis',(0.,0.,1.));
#5463=DIRECTION('center_axis',(0.,-1.,0.));
#5464=DIRECTION('ref_axis',(0.,0.,1.));
#5465=DIRECTION('center_axis',(0.,-1.,0.));
#5466=DIRECTION('ref_axis',(0.,0.,1.));
#5467=DIRECTION('center_axis',(0.,1.,0.));
#5468=DIRECTION('ref_axis',(0.,0.,-1.));
#5469=DIRECTION('center_axis',(0.,1.,0.));
#5470=DIRECTION('ref_axis',(0.,0.,-1.));
#5471=DIRECTION('center_axis',(0.,1.,0.));
#5472=DIRECTION('ref_axis',(0.,0.,-1.));
#5473=DIRECTION('center_axis',(0.,1.,0.));
#5474=DIRECTION('ref_axis',(0.,0.,-1.));
#5475=DIRECTION('center_axis',(0.,1.,0.));
#5476=DIRECTION('ref_axis',(0.,0.,-1.));
#5477=DIRECTION('center_axis',(0.,1.,0.));
#5478=DIRECTION('ref_axis',(0.,0.,-1.));
#9394=CARTESIAN_POINT('',(0.,0.,0.));
#9395=CARTESIAN_POINT('Origin',(6.,12.,10.3923048454133));
#9396=CARTESIAN_POINT('',(12.,1.60769515458673,-2.07311314789647E-15));
#9397=CARTESIAN_POINT('',(9.,0.,5.19615242270663));
#9398=CARTESIAN_POINT('Ctrl Pts',(11.9999999999992,1.60769515458591,1.42578261298065E-12));
#9399=CARTESIAN_POINT('Ctrl Pts',(10.3923048454129,1.11022302462516E-15,
2.7846096908271));
#9400=CARTESIAN_POINT('Ctrl Pts',(9.,2.73207272303746E-15,5.19615242270663));
#9401=CARTESIAN_POINT('',(12.,10.3923048454133,-3.39099245361938E-15));
#9402=CARTESIAN_POINT('',(12.,10.3923048454133,-3.61640635416958E-15));
#9403=CARTESIAN_POINT('',(9.,12.,5.19615242270663));
#9404=CARTESIAN_POINT('Ctrl Pts',(9.00000000000001,12.,5.19615242270662));
#9405=CARTESIAN_POINT('Ctrl Pts',(10.3923048454129,12.,2.78460969082709));
#9406=CARTESIAN_POINT('Ctrl Pts',(11.9999999999992,10.3923048454141,1.41342337334735E-12));
#9407=CARTESIAN_POINT('',(6.,10.3923048454133,10.3923048454133));
#9408=CARTESIAN_POINT('Ctrl Pts',(6.00000000000083,10.3923048454141,10.3923048454118));
#9409=CARTESIAN_POINT('Ctrl Pts',(7.60769515458707,12.,7.60769515458616));
#9410=CARTESIAN_POINT('Ctrl Pts',(9.00000000000001,12.,5.19615242270662));
#9411=CARTESIAN_POINT('',(6.00000000000079,1.6076951545867,10.3923048454133));
#9412=CARTESIAN_POINT('',(6.,10.3923048454133,10.3923048454133));
#9413=CARTESIAN_POINT('Ctrl Pts',(9.00000000000001,1.09283143764095E-15,
5.19615242270663));
#9414=CARTESIAN_POINT('Ctrl Pts',(7.60769515458714,2.37120928169226E-16,
7.60769515458605));
#9415=CARTESIAN_POINT('Ctrl Pts',(6.00000000000099,1.60769515458575,10.3923048454116));
#9416=CARTESIAN_POINT('Origin',(12.,12.,-3.61640635416958E-15));
#9417=CARTESIAN_POINT('',(6.,1.60769515458673,-10.3923048454133));
#9418=CARTESIAN_POINT('',(9.,0.,-5.19615242270663));
#9419=CARTESIAN_POINT('Ctrl Pts',(6.00000000000082,1.60769515458591,-10.3923048454118));
#9420=CARTESIAN_POINT('Ctrl Pts',(7.60769515458707,5.77315972805081E-15,
-7.60769515458617));
#9421=CARTESIAN_POINT('Ctrl Pts',(9.,4.91773090146743E-15,-5.19615242270664));
#9422=CARTESIAN_POINT('',(6.00000000000009,10.3923048454133,-10.3923048454133));
#9423=CARTESIAN_POINT('',(6.,10.3923048454133,-10.3923048454133));
#9424=CARTESIAN_POINT('',(9.00000000000001,12.,-5.19615242270663));
#9425=CARTESIAN_POINT('Ctrl Pts',(9.00000000000001,12.,-5.19615242270662));
#9426=CARTESIAN_POINT('Ctrl Pts',(7.60769515458708,12.,-7.60769515458614));
#9427=CARTESIAN_POINT('Ctrl Pts',(6.00000000000086,10.3923048454141,-10.3923048454118));
#9428=CARTESIAN_POINT('Ctrl Pts',(11.9999999999992,10.3923048454141,-1.43697061821777E-12));
#9429=CARTESIAN_POINT('Ctrl Pts',(10.3923048454129,12.,-2.7846096908271));
#9430=CARTESIAN_POINT('Ctrl Pts',(9.00000000000001,12.,-5.19615242270662));
#9431=CARTESIAN_POINT('Ctrl Pts',(9.,4.64453360997405E-15,-5.19615242270664));
#9432=CARTESIAN_POINT('Ctrl Pts',(10.3923048454129,4.94022392384109E-15,
-2.78460969082711));
#9433=CARTESIAN_POINT('Ctrl Pts',(11.9999999999992,1.60769515458591,-1.43226116924369E-12));
#9434=CARTESIAN_POINT('Origin',(6.,12.,-10.3923048454133));
#9435=CARTESIAN_POINT('',(-6.,1.60769515458673,-10.3923048454133));
#9436=CARTESIAN_POINT('',(0.,0.,-10.3923048454133));
#9437=CARTESIAN_POINT('Ctrl Pts',(-5.99999999999835,1.60769515458591,-10.3923048454133));
#9438=CARTESIAN_POINT('Ctrl Pts',(-2.78460969082587,6.43929354282591E-15,
-10.3923048454133));
#9439=CARTESIAN_POINT('Ctrl Pts',(-2.18565828465779E-15,6.55697485397336E-15,
-10.3923048454133));
#9440=CARTESIAN_POINT('',(-6.,10.3923048454133,-10.3923048454133));
#9441=CARTESIAN_POINT('',(-6.,10.3923048454133,-10.3923048454133));
#9442=CARTESIAN_POINT('',(0.,12.,-10.3923048454133));
#9443=CARTESIAN_POINT('Ctrl Pts',(2.62278997768546E-14,12.,-10.3923048454133));
#9444=CARTESIAN_POINT('Ctrl Pts',(-2.78460969082585,12.,-10.3923048454133));
#9445=CARTESIAN_POINT('Ctrl Pts',(-5.99999999999834,10.3923048454141,-10.3923048454133));
#9446=CARTESIAN_POINT('Ctrl Pts',(5.99999999999843,10.3923048454141,-10.3923048454133));
#9447=CARTESIAN_POINT('Ctrl Pts',(2.78460969082591,12.,-10.3923048454133));
#9448=CARTESIAN_POINT('Ctrl Pts',(2.62278997768546E-14,12.,-10.3923048454133));
#9449=CARTESIAN_POINT('Ctrl Pts',(-1.52996401269733E-14,3.82491003174334E-15,
-10.3923048454133));
#9450=CARTESIAN_POINT('Ctrl Pts',(2.78460969082586,6.26139843732123E-17,
-10.3923048454133));
#9451=CARTESIAN_POINT('Ctrl Pts',(5.99999999999836,1.60769515458591,-10.3923048454133));
#9452=CARTESIAN_POINT('Origin',(-6.,12.,-10.3923048454133));
#9453=CARTESIAN_POINT('',(-12.,1.60769515458673,-1.44959860074153E-16));
#9454=CARTESIAN_POINT('',(-9.,0.,-5.19615242270663));
#9455=CARTESIAN_POINT('Ctrl Pts',(-11.9999999999992,1.60769515458591,-1.42813733240754E-12));
#9456=CARTESIAN_POINT('Ctrl Pts',(-10.3923048454129,-6.66133814775094E-16,
-2.78460969082711));
#9457=CARTESIAN_POINT('Ctrl Pts',(-9.,1.63924363382248E-15,-5.19615242270664));
#9458=CARTESIAN_POINT('',(-12.,10.3923048454133,-1.19184216575765E-16));
#9459=CARTESIAN_POINT('',(-12.,10.3923048454133,1.23259516440783E-29));
#9460=CARTESIAN_POINT('',(-9.00000000000001,12.,-5.19615242270663));
#9461=CARTESIAN_POINT('Ctrl Pts',(-9.,12.,-5.19615242270663));
#9462=CARTESIAN_POINT('Ctrl Pts',(-10.3923048454129,12.,-2.7846096908271));
#9463=CARTESIAN_POINT('Ctrl Pts',(-11.9999999999992,10.3923048454141,-1.4246083146608E-12));
#9464=CARTESIAN_POINT('Ctrl Pts',(-6.00000000000082,10.3923048454141,-10.3923048454118));
#9465=CARTESIAN_POINT('Ctrl Pts',(-7.60769515458707,12.,-7.60769515458616));
#9466=CARTESIAN_POINT('Ctrl Pts',(-9.,12.,-5.19615242270663));
#9467=CARTESIAN_POINT('Ctrl Pts',(-9.00000000000001,6.55698862584572E-15,
-5.19615242270663));
#9468=CARTESIAN_POINT('Ctrl Pts',(-7.60769515458707,6.21840847038348E-15,
-7.60769515458617));
#9469=CARTESIAN_POINT('Ctrl Pts',(-6.00000000000082,1.60769515458592,-10.3923048454119));
#9470=CARTESIAN_POINT('Origin',(-12.,12.,1.23259516440783E-29));
#9471=CARTESIAN_POINT('',(-6.,1.60769515458673,10.3923048454133));
#9472=CARTESIAN_POINT('',(-9.,0.,5.19615242270663));
#9473=CARTESIAN_POINT('Ctrl Pts',(-6.00000000000082,1.60769515458591,10.3923048454118));
#9474=CARTESIAN_POINT('Ctrl Pts',(-7.60769515458707,-1.77635683940025E-15,
7.60769515458616));
#9475=CARTESIAN_POINT('Ctrl Pts',(-9.00000000000001,4.91773090146746E-15,
5.19615242270662));
#9476=CARTESIAN_POINT('',(-6.0000000000001,10.3923048454133,10.3923048454133));
#9477=CARTESIAN_POINT('',(-6.,10.3923048454133,10.3923048454133));
#9478=CARTESIAN_POINT('',(-9.00000000000001,12.,5.19615242270663));
#9479=CARTESIAN_POINT('Ctrl Pts',(-9.,12.,5.19615242270663));
#9480=CARTESIAN_POINT('Ctrl Pts',(-7.60769515458708,12.,7.60769515458614));
#9481=CARTESIAN_POINT('Ctrl Pts',(-6.00000000000085,10.3923048454141,10.3923048454118));
#9482=CARTESIAN_POINT('Ctrl Pts',(-11.9999999999992,10.3923048454141,1.42931776363488E-12));
#9483=CARTESIAN_POINT('Ctrl Pts',(-10.3923048454129,12.,2.7846096908271));
#9484=CARTESIAN_POINT('Ctrl Pts',(-9.,12.,5.19615242270663));
#9485=CARTESIAN_POINT('Ctrl Pts',(-9.00000000000001,5.46415718820513E-16,
5.19615242270661));
#9486=CARTESIAN_POINT('Ctrl Pts',(-10.3923048454129,8.17530773838345E-15,
2.78460969082708));
#9487=CARTESIAN_POINT('Ctrl Pts',(-11.9999999999992,1.60769515458592,1.41165732998206E-12));
#9488=CARTESIAN_POINT('Origin',(-6.,12.,10.3923048454133));
#9489=CARTESIAN_POINT('',(-1.50231459873716E-15,0.,10.3923048454133));
#9490=CARTESIAN_POINT('Ctrl Pts',(5.99999999999897,1.60769515458622,10.3923048454133));
#9491=CARTESIAN_POINT('Ctrl Pts',(2.78460969082611,3.10862446895044E-15,
10.3923048454133));
#9492=CARTESIAN_POINT('Ctrl Pts',(-1.09282914232889E-15,3.00528014140446E-15,
10.3923048454133));
#9493=CARTESIAN_POINT('',(-1.73472347597681E-15,12.,10.3923048454133));
#9494=CARTESIAN_POINT('Ctrl Pts',(-2.34958268834322E-14,12.,10.3923048454133));
#9495=CARTESIAN_POINT('Ctrl Pts',(2.78460969082586,12.,10.3923048454133));
#9496=CARTESIAN_POINT('Ctrl Pts',(5.99999999999836,10.3923048454141,10.3923048454133));
#9497=CARTESIAN_POINT('Ctrl Pts',(-5.99999999999843,10.3923048454141,10.3923048454133));
#9498=CARTESIAN_POINT('Ctrl Pts',(-2.78460969082591,12.,10.3923048454133));
#9499=CARTESIAN_POINT('Ctrl Pts',(-2.34958268834322E-14,12.,10.3923048454133));
#9500=CARTESIAN_POINT('Ctrl Pts',(6.55698862584571E-15,8.19623578230717E-16,
10.3923048454133));
#9501=CARTESIAN_POINT('Ctrl Pts',(-2.78460969082587,-1.06903685822888E-15,
10.3923048454133));
#9502=CARTESIAN_POINT('Ctrl Pts',(-5.99999999999837,1.60769515458591,10.3923048454133));
#9503=CARTESIAN_POINT('Origin',(0.,0.,0.));
#9504=CARTESIAN_POINT('Origin',(0.,0.,0.));
#9505=CARTESIAN_POINT('Origin',(0.,0.,0.));
#9506=CARTESIAN_POINT('Origin',(0.,0.,0.));
#9507=CARTESIAN_POINT('Origin',(0.,0.,0.));
#9508=CARTESIAN_POINT('Origin',(0.,0.,0.));
#9509=CARTESIAN_POINT('Origin',(0.,0.,0.));
#9510=CARTESIAN_POINT('',(0.,0.,6.));
#9511=CARTESIAN_POINT('Origin',(0.,0.,0.));
#9512=CARTESIAN_POINT('Origin',(0.,12.,0.));
#9513=CARTESIAN_POINT('Origin',(0.,12.,0.));
#9514=CARTESIAN_POINT('Origin',(0.,12.,0.));
#9515=CARTESIAN_POINT('Origin',(0.,12.,0.));
#9516=CARTESIAN_POINT('Origin',(0.,12.,0.));
#9517=CARTESIAN_POINT('Origin',(0.,12.,0.));
#9518=CARTESIAN_POINT('Origin',(0.,12.,0.));
#9519=CARTESIAN_POINT('',(0.,12.,6.));
#9520=CARTESIAN_POINT('Origin',(0.,12.,0.));
#9521=CARTESIAN_POINT('Origin',(0.,12.,0.));
#9522=CARTESIAN_POINT('',(-7.34788079488412E-16,12.,6.));
#9523=CARTESIAN_POINT('Origin',(0.,12.,0.));
#9524=CARTESIAN_POINT('Origin',(0.,12.,0.));
#9525=CARTESIAN_POINT('Origin',(0.,12.,0.));
#9526=CARTESIAN_POINT('Origin',(0.,12.,0.));
#9527=CARTESIAN_POINT('Origin',(0.,12.,0.));
#9528=CARTESIAN_POINT('Origin',(0.,12.,0.));
#9529=CARTESIAN_POINT('Origin',(0.,0.,0.));
#9530=CARTESIAN_POINT('Origin',(0.,0.,0.));
#9531=CARTESIAN_POINT('Origin',(0.,0.,0.));
#9532=CARTESIAN_POINT('Origin',(0.,0.,0.));
#9533=CARTESIAN_POINT('Origin',(0.,0.,0.));
#9534=CARTESIAN_POINT('Origin',(0.,0.,0.));
#9653=UNCERTAINTY_MEASURE_WITH_UNIT(LENGTH_MEASURE(0.01),#9669,
'DISTANCE_ACCURACY_VALUE',
'Maximum model space distance between geometric entities at asserted c
onnectivities');
#9655=UNCERTAINTY_MEASURE_WITH_UNIT(LENGTH_MEASURE(0.01),#9669,
'DISTANCE_ACCURACY_VALUE',
'Maximum model space distance between geometric entities at asserted c
onnectivities');
#9666=(
GEOMETRIC_REPRESENTATION_CONTEXT(3)
GLOBAL_UNCERTAINTY_ASSIGNED_CONTEXT((#9653))
GLOBAL_UNIT_ASSIGNED_CONTEXT((#9669,#9671,#9672))
REPRESENTATION_CONTEXT('','3D')
);
#9668=(
GEOMETRIC_REPRESENTATION_CONTEXT(3)
GLOBAL_UNCERTAINTY_ASSIGNED_CONTEXT((#9655))
GLOBAL_UNIT_ASSIGNED_CONTEXT((#9669,#9671,#9672))
REPRESENTATION_CONTEXT('','3D')
);
#9669=(
LENGTH_UNIT()
NAMED_UNIT(*)
SI_UNIT(.MILLI.,.METRE.)
);
#9671=(
NAMED_UNIT(*)
PLANE_ANGLE_UNIT()
SI_UNIT($,.RADIAN.)
);
#9672=(
NAMED_UNIT(*)
SI_UNIT($,.STERADIAN.)
SOLID_ANGLE_UNIT()
);
#9683=SHAPE_DEFINITION_REPRESENTATION(#9695,#9721);
#9695=PRODUCT_DEFINITION_SHAPE('',$,#9734);
#9721=SHAPE_REPRESENTATION('',(#4394),#9666);
#9723=PRODUCT_DEFINITION_CONTEXT('part definition',#9761,'design');
#9734=PRODUCT_DEFINITION('2026-10-04-08-13-48-889','NUT',#9746,#9723);
#9746=PRODUCT_DEFINITION_FORMATION('',$,#9773);
#9761=APPLICATION_CONTEXT(
'Core Data for Automotive Mechanical Design Process');
#9762=PRODUCT_CONTEXT('part definition',#9761,'mechanical');
#9773=PRODUCT('2026-10-04-08-13-48-889','NUT','PART',(#9762));
#9775=PRESENTATION_STYLE_ASSIGNMENT((#9776));
#9776=SURFACE_STYLE_USAGE(.BOTH.,#9777);
#9777=SURFACE_SIDE_STYLE('',(#9778));
#9778=SURFACE_STYLE_FILL_AREA(#9779);
#9779=FILL_AREA_STYLE('Steel - Satin',(#9780));
#9780=FILL_AREA_STYLE_COLOUR('Steel - Satin',#9781);
#9781=COLOUR_RGB('Steel - Satin', 0.09019608, 0.27058824, 0.51372549);
ENDSEC;
END-ISO-10303-21;
